ISO-10303-21;
HEADER;
/* Generated by software containing ST-Developer
 * from STEP Tools, Inc. (www.steptools.com) 
 */

FILE_DESCRIPTION(
/* description */ ('PAT-091'),
/* implementation_level */ '2;1');

FILE_NAME(
/* name */ 'Axle distance sleeve 5 mm (11).step',
/* time_stamp */ '2026-10-27T15:34:44-07:00',
/* author */ (''),
/* organization */ (''),
/* preprocessor_version */ 'ST-DEVELOPER v20.2',
/* originating_system */ 'Autodesk Translation Framework v15.17.0.0',
/* authorisation */ '');

FILE_SCHEMA (('AUTOMOTIVE_DESIGN { 1 0 10303 214 3 1 1 }'));
ENDSEC;

DATA;
#10=MECHANICAL_DESIGN_GEOMETRIC_PRESENTATION_REPRESENTATION('',(#1042),#25100);
#822=SHAPE_REPRESENTATION_RELATIONSHIP('SRR','None',#25588,#932);
#932=ADVANCED_BREP_SHAPE_REPRESENTATION('',(#1164),#25058);
#1042=STYLED_ITEM('',(#26191),#1164);
#1164=MANIFOLD_SOLID_BREP('Body1',#13321);
#1522=FACE_BOUND('',#3720,.T.);
#1523=FACE_BOUND('',#3722,.T.);
#1935=PLANE('',#15671);
#1936=PLANE('',#15672);
#2592=FACE_OUTER_BOUND('',#3717,.T.);
#2593=FACE_OUTER_BOUND('',#3718,.T.);
#2594=FACE_OUTER_BOUND('',#3719,.T.);
#2595=FACE_OUTER_BOUND('',#3721,.T.);
#3717=EDGE_LOOP('',(#11068,#11069,#11070,#11071));
#3718=EDGE_LOOP('',(#11072,#11073,#11074,#11075));
#3719=EDGE_LOOP('',(#11076));
#3720=EDGE_LOOP('',(#11077));
#3721=EDGE_LOOP('',(#11078));
#3722=EDGE_LOOP('',(#11079));
#4698=LINE('',#23384,#5438);
#4699=LINE('',#23390,#5439);
#5438=VECTOR('',#19206,0.605);
#5439=VECTOR('',#19213,0.800000000000001);
#6074=CIRCLE('',#15666,0.605);
#6075=CIRCLE('',#15667,0.605);
#6076=CIRCLE('',#15669,0.800000000000001);
#6077=CIRCLE('',#15670,0.800000000000001);
#7079=VERTEX_POINT('',#23381);
#7080=VERTEX_POINT('',#23383);
#7081=VERTEX_POINT('',#23387);
#7082=VERTEX_POINT('',#23389);
#8469=EDGE_CURVE('',#7079,#7079,#6074,.T.);
#8470=EDGE_CURVE('',#7079,#7080,#4698,.T.);
#8471=EDGE_CURVE('',#7080,#7080,#6075,.T.);
#8472=EDGE_CURVE('',#7081,#7081,#6076,.T.);
#8473=EDGE_CURVE('',#7081,#7082,#4699,.T.);
#8474=EDGE_CURVE('',#7082,#7082,#6077,.T.);
#11068=ORIENTED_EDGE('',*,*,#8469,.F.);
#11069=ORIENTED_EDGE('',*,*,#8470,.T.);
#11070=ORIENTED_EDGE('',*,*,#8471,.T.);
#11071=ORIENTED_EDGE('',*,*,#8470,.F.);
#11072=ORIENTED_EDGE('',*,*,#8472,.F.);
#11073=ORIENTED_EDGE('',*,*,#8473,.T.);
#11074=ORIENTED_EDGE('',*,*,#8474,.T.);
#11075=ORIENTED_EDGE('',*,*,#8473,.F.);
#11076=ORIENTED_EDGE('',*,*,#8472,.T.);
#11077=ORIENTED_EDGE('',*,*,#8469,.T.);
#11078=ORIENTED_EDGE('',*,*,#8474,.F.);
#11079=ORIENTED_EDGE('',*,*,#8471,.F.);
#12300=CYLINDRICAL_SURFACE('',#15665,0.605);
#12301=CYLINDRICAL_SURFACE('',#15668,0.800000000000001);
#12959=ADVANCED_FACE('',(#2592),#12300,.F.);
#12960=ADVANCED_FACE('',(#2593),#12301,.T.);
#12961=ADVANCED_FACE('',(#2594,#1522),#1935,.T.);
#12962=ADVANCED_FACE('',(#2595,#1523),#1936,.F.);
#13321=CLOSED_SHELL('',(#12959,#12960,#12961,#12962));
#15664=AXIS2_PLACEMENT_3D('',#23379,#19200,#19201);
#15665=AXIS2_PLACEMENT_3D('',#23380,#19202,#19203);
#15666=AXIS2_PLACEMENT_3D('',#23382,#19204,#19205);
#15667=AXIS2_PLACEMENT_3D('',#23385,#19207,#19208);
#15668=AXIS2_PLACEMENT_3D('',#23386,#19209,#19210);
#15669=AXIS2_PLACEMENT_3D('',#23388,#19211,#19212);
#15670=AXIS2_PLACEMENT_3D('',#23391,#19214,#19215);
#15671=AXIS2_PLACEMENT_3D('',#23392,#19216,#19217);
#15672=AXIS2_PLACEMENT_3D('',#23393,#19218,#19219);
#19200=DIRECTION('axis',(0.,0.,1.));
#19201=DIRECTION('refdir',(1.,0.,0.));
#19202=DIRECTION('center_axis',(0.,1.,0.));
#19203=DIRECTION('ref_axis',(1.,0.,0.));
#19204=DIRECTION('center_axis',(0.,-1.,0.));
#19205=DIRECTION('ref_axis',(1.,0.,0.));
#19206=DIRECTION('',(0.,-1.,0.));
#19207=DIRECTION('center_axis',(0.,-1.,0.));
#19208=DIRECTION('ref_axis',(1.,0.,0.));
#19209=DIRECTION('center_axis',(0.,1.,0.));
#19210=DIRECTION('ref_axis',(1.,0.,0.));
#19211=DIRECTION('center_axis',(0.,1.,0.));
#19212=DIRECTION('ref_axis',(1.,0.,0.));
#19213=DIRECTION('',(0.,-1.,0.));
#19214=DIRECTION('center_axis',(0.,1.,0.));
#19215=DIRECTION('ref_axis',(1.,0.,0.));
#19216=DIRECTION('center_axis',(0.,1.,0.));
#19217=DIRECTION('ref_axis',(1.,0.,0.));
#19218=DIRECTION('center_axis',(0.,1.,0.));
#19219=DIRECTION('ref_axis',(1.,0.,0.));
#23379=CARTESIAN_POINT('',(0.,0.,0.));
#23380=CARTESIAN_POINT('Origin',(19.3649167310371,8.,8.));
#23381=CARTESIAN_POINT('',(18.7599167310371,8.5,8.));
#23382=CARTESIAN_POINT('Origin',(19.3649167310371,8.5,8.));
#23383=CARTESIAN_POINT('',(18.7599167310371,8.,8.));
#23384=CARTESIAN_POINT('',(18.7599167310371,8.,8.));
#23385=CARTESIAN_POINT('Origin',(19.3649167310371,8.,8.));
#23386=CARTESIAN_POINT('Origin',(19.3649167310371,8.,8.));
#23387=CARTESIAN_POINT('',(18.5649167310371,8.5,8.));
#23388=CARTESIAN_POINT('Origin',(19.3649167310371,8.5,8.));
#23389=CARTESIAN_POINT('',(18.5649167310371,8.,8.));
#23390=CARTESIAN_POINT('',(18.5649167310371,8.,8.));
#23391=CARTESIAN_POINT('Origin',(19.3649167310371,8.,8.));
#23392=CARTESIAN_POINT('Origin',(19.3649167310371,8.5,8.));
#23393=CARTESIAN_POINT('Origin',(19.3649167310371,8.,8.));
#24937=UNCERTAINTY_MEASURE_WITH_UNIT(LENGTH_MEASURE(0.001),#25101,
'DISTANCE_ACCURACY_VALUE',
'Maximum model space distance between geometric entities at asserted c
onnectivities');
#24979=UNCERTAINTY_MEASURE_WITH_UNIT(LENGTH_MEASURE(0.001),#25101,
'DISTANCE_ACCURACY_VALUE',
'Maximum model space distance between geometric entities at asserted c
onnectivities');
#25058=(
GEOMETRIC_REPRESENTATION_CONTEXT(3)
GLOBAL_UNCERTAINTY_ASSIGNED_CONTEXT((#24937))
GLOBAL_UNIT_ASSIGNED_CONTEXT((#25101,#25103,#25104))
REPRESENTATION_CONTEXT('','3D')
);
#25100=(
GEOMETRIC_REPRESENTATION_CONTEXT(3)
GLOBAL_UNCERTAINTY_ASSIGNED_CONTEXT((#24979))
GLOBAL_UNIT_ASSIGNED_CONTEXT((#25101,#25103,#25104))
REPRESENTATION_CONTEXT('','3D')
);
#25101=(
LENGTH_UNIT()
NAMED_UNIT(*)
SI_UNIT(.CENTI.,.METRE.)
);
#25103=(
NAMED_UNIT(*)
PLANE_ANGLE_UNIT()
SI_UNIT($,.RADIAN.)
);
#25104=(
NAMED_UNIT(*)
SI_UNIT($,.STERADIAN.)
SOLID_ANGLE_UNIT()
);
#25183=SHAPE_DEFINITION_REPRESENTATION(#25305,#25588);
#25305=PRODUCT_DEFINITION_SHAPE('',$,#25709);
#25588=SHAPE_REPRESENTATION('',(#15664),#25058);
#25630=PRODUCT_DEFINITION_CONTEXT('part definition',#25992,'design');
#25709=PRODUCT_DEFINITION('Axle distance sleeve 5 mm (11)',
'Axle distance sleeve 5 mm (11)',#25829,#25630);
#25829=PRODUCT_DEFINITION_FORMATION('',$,#26072);
#25992=APPLICATION_CONTEXT(
'Core Data for Automotive Mechanical Design Process');
#25993=PRODUCT_CONTEXT('part definition',#25992,'mechanical');
#26072=PRODUCT('Axle distance sleeve 5 mm (11)',
'Axle distance sleeve 5 mm (11)','Axle distance sleeve 5 mm (11)',(#25993));
#26185=COLOUR_RGB('Grey',0.48,0.52,0.57);
#26186=FILL_AREA_STYLE_COLOUR('',#26185);
#26187=FILL_AREA_STYLE('',(#26186));
#26188=SURFACE_STYLE_FILL_AREA(#26187);
#26189=SURFACE_SIDE_STYLE('',(#26188));
#26190=SURFACE_STYLE_USAGE(.BOTH.,#26189);
#26191=PRESENTATION_STYLE_ASSIGNMENT((#26190));
ENDSEC;
END-ISO-10303-21;
